ISO-10303-21;
HEADER;
/* Generated by software containing ST-Developer
 * from STEP Tools, Inc. (www.steptools.com) 
 */

FILE_DESCRIPTION(
/* description */ ('Turntable on roller ring'),
/* implementation_level */ '2;1');

FILE_NAME(
/* name */ 'Balls (1).step',
/* time_stamp */ '2026-10-28T03:23:59-07:00',
/* author */ (''),
/* organization */ (''),
/* preprocessor_version */ 'ST-DEVELOPER v20.2',
/* originating_system */ 'Autodesk Translation Framework v15.17.0.0',
/* authorisation */ '');

FILE_SCHEMA (('AUTOMOTIVE_DESIGN { 1 0 10303 214 3 1 1 }'));
ENDSEC;

DATA;
#10=MECHANICAL_DESIGN_GEOMETRIC_PRESENTATION_REPRESENTATION('',(#678,#679,#680,#681,#682,#683,#684,#685),#16281);
#456=SPHERICAL_SURFACE('',#10082,0.23815);
#457=SPHERICAL_SURFACE('',#10084,0.23815);
#458=SPHERICAL_SURFACE('',#10086,0.23815);
#459=SPHERICAL_SURFACE('',#10088,0.23815);
#460=SPHERICAL_SURFACE('',#10090,0.23815);
#461=SPHERICAL_SURFACE('',#10092,0.23815);
#462=SPHERICAL_SURFACE('',#10094,0.23815);
#463=SPHERICAL_SURFACE('',#10096,0.23815);
#559=SHAPE_REPRESENTATION_RELATIONSHIP('SRR','None',#16584,#614);
#614=ADVANCED_BREP_SHAPE_REPRESENTATION('',(#746,#747,#748,#749,#750,#751,
#752,#753),#16278);
#678=STYLED_ITEM('',(#16932),#746);
#679=STYLED_ITEM('',(#16932),#747);
#680=STYLED_ITEM('',(#16932),#748);
#681=STYLED_ITEM('',(#16932),#749);
#682=STYLED_ITEM('',(#16932),#750);
#683=STYLED_ITEM('',(#16932),#751);
#684=STYLED_ITEM('',(#16932),#752);
#685=STYLED_ITEM('',(#16932),#753);
#746=MANIFOLD_SOLID_BREP('Body1',#8423);
#747=MANIFOLD_SOLID_BREP('Body2',#8424);
#748=MANIFOLD_SOLID_BREP('Body3',#8425);
#749=MANIFOLD_SOLID_BREP('Body4',#8426);
#750=MANIFOLD_SOLID_BREP('Body5',#8427);
#751=MANIFOLD_SOLID_BREP('Body6',#8428);
#752=MANIFOLD_SOLID_BREP('Body7',#8429);
#753=MANIFOLD_SOLID_BREP('Body8',#8430);
#1720=FACE_OUTER_BOUND('',#2453,.T.);
#1721=FACE_OUTER_BOUND('',#2454,.T.);
#1722=FACE_OUTER_BOUND('',#2455,.T.);
#1723=FACE_OUTER_BOUND('',#2456,.T.);
#1724=FACE_OUTER_BOUND('',#2457,.T.);
#1725=FACE_OUTER_BOUND('',#2458,.T.);
#1726=FACE_OUTER_BOUND('',#2459,.T.);
#1727=FACE_OUTER_BOUND('',#2460,.T.);
#2453=EDGE_LOOP('',(#7521,#7522));
#2454=EDGE_LOOP('',(#7523,#7524));
#2455=EDGE_LOOP('',(#7525,#7526));
#2456=EDGE_LOOP('',(#7527,#7528));
#2457=EDGE_LOOP('',(#7529,#7530));
#2458=EDGE_LOOP('',(#7531,#7532));
#2459=EDGE_LOOP('',(#7533,#7534));
#2460=EDGE_LOOP('',(#7535,#7536));
#3899=CIRCLE('',#10083,0.23815);
#3900=CIRCLE('',#10085,0.23815);
#3901=CIRCLE('',#10087,0.23815);
#3902=CIRCLE('',#10089,0.23815);
#3903=CIRCLE('',#10091,0.23815);
#3904=CIRCLE('',#10093,0.23815);
#3905=CIRCLE('',#10095,0.23815);
#3906=CIRCLE('',#10097,0.23815);
#4573=VERTEX_POINT('',#15605);
#4574=VERTEX_POINT('',#15606);
#4575=VERTEX_POINT('',#15609);
#4576=VERTEX_POINT('',#15610);
#4577=VERTEX_POINT('',#15613);
#4578=VERTEX_POINT('',#15614);
#4579=VERTEX_POINT('',#15617);
#4580=VERTEX_POINT('',#15618);
#4581=VERTEX_POINT('',#15621);
#4582=VERTEX_POINT('',#15622);
#4583=VERTEX_POINT('',#15625);
#4584=VERTEX_POINT('',#15626);
#4585=VERTEX_POINT('',#15629);
#4586=VERTEX_POINT('',#15630);
#4587=VERTEX_POINT('',#15633);
#4588=VERTEX_POINT('',#15634);
#5571=EDGE_CURVE('',#4573,#4574,#3899,.T.);
#5572=EDGE_CURVE('',#4575,#4576,#3900,.T.);
#5573=EDGE_CURVE('',#4577,#4578,#3901,.T.);
#5574=EDGE_CURVE('',#4579,#4580,#3902,.T.);
#5575=EDGE_CURVE('',#4581,#4582,#3903,.T.);
#5576=EDGE_CURVE('',#4583,#4584,#3904,.T.);
#5577=EDGE_CURVE('',#4585,#4586,#3905,.T.);
#5578=EDGE_CURVE('',#4587,#4588,#3906,.T.);
#7521=ORIENTED_EDGE('',*,*,#5571,.T.);
#7522=ORIENTED_EDGE('',*,*,#5571,.F.);
#7523=ORIENTED_EDGE('',*,*,#5572,.T.);
#7524=ORIENTED_EDGE('',*,*,#5572,.F.);
#7525=ORIENTED_EDGE('',*,*,#5573,.T.);
#7526=ORIENTED_EDGE('',*,*,#5573,.F.);
#7527=ORIENTED_EDGE('',*,*,#5574,.T.);
#7528=ORIENTED_EDGE('',*,*,#5574,.F.);
#7529=ORIENTED_EDGE('',*,*,#5575,.T.);
#7530=ORIENTED_EDGE('',*,*,#5575,.F.);
#7531=ORIENTED_EDGE('',*,*,#5576,.T.);
#7532=ORIENTED_EDGE('',*,*,#5576,.F.);
#7533=ORIENTED_EDGE('',*,*,#5577,.T.);
#7534=ORIENTED_EDGE('',*,*,#5577,.F.);
#7535=ORIENTED_EDGE('',*,*,#5578,.T.);
#7536=ORIENTED_EDGE('',*,*,#5578,.F.);
#8323=ADVANCED_FACE('',(#1720),#456,.T.);
#8324=ADVANCED_FACE('',(#1721),#457,.T.);
#8325=ADVANCED_FACE('',(#1722),#458,.T.);
#8326=ADVANCED_FACE('',(#1723),#459,.T.);
#8327=ADVANCED_FACE('',(#1724),#460,.T.);
#8328=ADVANCED_FACE('',(#1725),#461,.T.);
#8329=ADVANCED_FACE('',(#1726),#462,.T.);
#8330=ADVANCED_FACE('',(#1727),#463,.T.);
#8423=CLOSED_SHELL('',(#8323));
#8424=CLOSED_SHELL('',(#8324));
#8425=CLOSED_SHELL('',(#8325));
#8426=CLOSED_SHELL('',(#8326));
#8427=CLOSED_SHELL('',(#8327));
#8428=CLOSED_SHELL('',(#8328));
#8429=CLOSED_SHELL('',(#8329));
#8430=CLOSED_SHELL('',(#8330));
#10081=AXIS2_PLACEMENT_3D('',#15603,#12759,#12760);
#10082=AXIS2_PLACEMENT_3D('',#15604,#12761,#12762);
#10083=AXIS2_PLACEMENT_3D('',#15607,#12763,#12764);
#10084=AXIS2_PLACEMENT_3D('',#15608,#12765,#12766);
#10085=AXIS2_PLACEMENT_3D('',#15611,#12767,#12768);
#10086=AXIS2_PLACEMENT_3D('',#15612,#12769,#12770);
#10087=AXIS2_PLACEMENT_3D('',#15615,#12771,#12772);
#10088=AXIS2_PLACEMENT_3D('',#15616,#12773,#12774);
#10089=AXIS2_PLACEMENT_3D('',#15619,#12775,#12776);
#10090=AXIS2_PLACEMENT_3D('',#15620,#12777,#12778);
#10091=AXIS2_PLACEMENT_3D('',#15623,#12779,#12780);
#10092=AXIS2_PLACEMENT_3D('',#15624,#12781,#12782);
#10093=AXIS2_PLACEMENT_3D('',#15627,#12783,#12784);
#10094=AXIS2_PLACEMENT_3D('',#15628,#12785,#12786);
#10095=AXIS2_PLACEMENT_3D('',#15631,#12787,#12788);
#10096=AXIS2_PLACEMENT_3D('',#15632,#12789,#12790);
#10097=AXIS2_PLACEMENT_3D('',#15635,#12791,#12792);
#12759=DIRECTION('axis',(0.,0.,1.));
#12760=DIRECTION('refdir',(1.,0.,0.));
#12761=DIRECTION('center_axis',(0.,0.,1.));
#12762=DIRECTION('ref_axis',(1.,0.,0.));
#12763=DIRECTION('center_axis',(1.22464679914735E-16,-1.,0.));
#12764=DIRECTION('ref_axis',(-1.,-1.22464679914735E-16,0.));
#12765=DIRECTION('center_axis',(0.707106781186548,0.,0.707106781186548));
#12766=DIRECTION('ref_axis',(0.707106781186548,0.,-0.707106781186548));
#12767=DIRECTION('center_axis',(8.65956056235494E-17,-1.,-8.65956056235493E-17));
#12768=DIRECTION('ref_axis',(-0.707106781186547,-1.22464679914735E-16,0.707106781186547));
#12769=DIRECTION('center_axis',(1.,0.,0.));
#12770=DIRECTION('ref_axis',(6.12323399573676E-17,0.,-1.));
#12771=DIRECTION('center_axis',(7.49879891330929E-33,-1.,-1.22464679914735E-16));
#12772=DIRECTION('ref_axis',(-6.12323399573676E-17,-1.22464679914735E-16,
1.));
#12773=DIRECTION('center_axis',(0.707106781186548,0.,-0.707106781186548));
#12774=DIRECTION('ref_axis',(-0.707106781186548,0.,-0.707106781186548));
#12775=DIRECTION('center_axis',(-8.65956056235493E-17,-1.,-8.65956056235494E-17));
#12776=DIRECTION('ref_axis',(0.707106781186547,-1.22464679914735E-16,0.707106781186547));
#12777=DIRECTION('center_axis',(0.,0.,-1.));
#12778=DIRECTION('ref_axis',(-1.,0.,-1.22464679914735E-16));
#12779=DIRECTION('center_axis',(-1.22464679914735E-16,-1.,-1.49975978266186E-32));
#12780=DIRECTION('ref_axis',(1.,-1.22464679914735E-16,1.22464679914735E-16));
#12781=DIRECTION('center_axis',(-0.707106781186547,0.,-0.707106781186548));
#12782=DIRECTION('ref_axis',(-0.707106781186548,0.,0.707106781186547));
#12783=DIRECTION('center_axis',(-8.65956056235493E-17,-1.,8.65956056235493E-17));
#12784=DIRECTION('ref_axis',(0.707106781186548,-1.22464679914735E-16,-0.707106781186547));
#12785=DIRECTION('center_axis',(-1.,0.,0.));
#12786=DIRECTION('ref_axis',(-1.83697019872103E-16,0.,1.));
#12787=DIRECTION('center_axis',(-2.24963967399279E-32,-1.,1.22464679914735E-16));
#12788=DIRECTION('ref_axis',(1.83697019872103E-16,-1.22464679914735E-16,
-1.));
#12789=DIRECTION('center_axis',(-0.707106781186548,0.,0.707106781186548));
#12790=DIRECTION('ref_axis',(0.707106781186547,0.,0.707106781186548));
#12791=DIRECTION('center_axis',(8.65956056235493E-17,-1.,8.65956056235493E-17));
#12792=DIRECTION('ref_axis',(-0.707106781186547,-1.22464679914735E-16,-0.707106781186548));
#15603=CARTESIAN_POINT('',(0.,0.,0.));
#15604=CARTESIAN_POINT('Origin',(1.,0.,0.));
#15605=CARTESIAN_POINT('',(1.,-1.78583896120461E-33,0.23815));
#15606=CARTESIAN_POINT('',(1.,-1.78583896120461E-33,-0.23815));
#15607=CARTESIAN_POINT('Origin',(1.,0.,0.));
#15608=CARTESIAN_POINT('Origin',(0.707106781186548,0.,-0.707106781186547));
#15609=CARTESIAN_POINT('',(0.875504261126124,-1.78583896120461E-33,-0.538709301246971));
#15610=CARTESIAN_POINT('',(0.538709301246971,-1.78583896120461E-33,-0.875504261126124));
#15611=CARTESIAN_POINT('Origin',(0.707106781186548,0.,-0.707106781186547));
#15612=CARTESIAN_POINT('Origin',(6.12323399573677E-17,0.,-1.));
#15613=CARTESIAN_POINT('',(0.23815,-1.78583896120461E-33,-1.));
#15614=CARTESIAN_POINT('',(-0.23815,-1.78583896120461E-33,-1.));
#15615=CARTESIAN_POINT('Origin',(6.12323399573677E-17,0.,-1.));
#15616=CARTESIAN_POINT('Origin',(-0.707106781186547,0.,-0.707106781186548));
#15617=CARTESIAN_POINT('',(-0.538709301246971,-1.78583896120461E-33,-0.875504261126124));
#15618=CARTESIAN_POINT('',(-0.875504261126124,-1.78583896120461E-33,-0.538709301246971));
#15619=CARTESIAN_POINT('Origin',(-0.707106781186547,0.,-0.707106781186548));
#15620=CARTESIAN_POINT('Origin',(-1.,0.,-1.22464679914735E-16));
#15621=CARTESIAN_POINT('',(-1.,-1.78583896120461E-33,-0.23815));
#15622=CARTESIAN_POINT('',(-1.,-1.78583896120461E-33,0.23815));
#15623=CARTESIAN_POINT('Origin',(-1.,0.,-1.22464679914735E-16));
#15624=CARTESIAN_POINT('Origin',(-0.707106781186548,0.,0.707106781186547));
#15625=CARTESIAN_POINT('',(-0.875504261126124,-7.94881478324376E-33,0.538709301246971));
#15626=CARTESIAN_POINT('',(-0.538709301246971,4.37713686083455E-33,0.875504261126124));
#15627=CARTESIAN_POINT('Origin',(-0.707106781186548,0.,0.707106781186547));
#15628=CARTESIAN_POINT('Origin',(-1.83697019872103E-16,0.,1.));
#15629=CARTESIAN_POINT('',(-0.23815,-1.78583896120461E-33,1.));
#15630=CARTESIAN_POINT('',(0.23815,-1.78583896120461E-33,1.));
#15631=CARTESIAN_POINT('Origin',(-1.83697019872103E-16,0.,1.));
#15632=CARTESIAN_POINT('Origin',(0.707106781186547,0.,0.707106781186548));
#15633=CARTESIAN_POINT('',(0.538709301246971,-4.86732687222419E-33,0.875504261126124));
#15634=CARTESIAN_POINT('',(0.875504261126124,1.29564894981497E-33,0.538709301246971));
#15635=CARTESIAN_POINT('Origin',(0.707106781186547,0.,0.707106781186548));
#16209=UNCERTAINTY_MEASURE_WITH_UNIT(LENGTH_MEASURE(0.001),#16282,
'DISTANCE_ACCURACY_VALUE',
'Maximum model space distance between geometric entities at asserted c
onnectivities');
#16212=UNCERTAINTY_MEASURE_WITH_UNIT(LENGTH_MEASURE(0.001),#16282,
'DISTANCE_ACCURACY_VALUE',
'Maximum model space distance between geometric entities at asserted c
onnectivities');
#16278=(
GEOMETRIC_REPRESENTATION_CONTEXT(3)
GLOBAL_UNCERTAINTY_ASSIGNED_CONTEXT((#16209))
GLOBAL_UNIT_ASSIGNED_CONTEXT((#16282,#16284,#16285))
REPRESENTATION_CONTEXT('','3D')
);
#16281=(
GEOMETRIC_REPRESENTATION_CONTEXT(3)
GLOBAL_UNCERTAINTY_ASSIGNED_CONTEXT((#16212))
GLOBAL_UNIT_ASSIGNED_CONTEXT((#16282,#16284,#16285))
REPRESENTATION_CONTEXT('','3D')
);
#16282=(
LENGTH_UNIT()
NAMED_UNIT(*)
SI_UNIT(.CENTI.,.METRE.)
);
#16284=(
NAMED_UNIT(*)
PLANE_ANGLE_UNIT()
SI_UNIT($,.RADIAN.)
);
#16285=(
NAMED_UNIT(*)
SI_UNIT($,.STERADIAN.)
SOLID_ANGLE_UNIT()
);
#16351=SHAPE_DEFINITION_REPRESENTATION(#16485,#16584);
#16485=PRODUCT_DEFINITION_SHAPE('',$,#16653);
#16584=SHAPE_REPRESENTATION('',(#10081),#16278);
#16587=PRODUCT_DEFINITION_CONTEXT('part definition',#16793,'design');
#16653=PRODUCT_DEFINITION('Balls (1)','Balls (1)',#16721,#16587);
#16721=PRODUCT_DEFINITION_FORMATION('',$,#16860);
#16793=APPLICATION_CONTEXT(
'Core Data for Automotive Mechanical Design Process');
#16794=PRODUCT_CONTEXT('part definition',#16793,'mechanical');
#16860=PRODUCT('Balls (1)','Balls (1)','Balls (1)',(#16794));
#16926=COLOUR_RGB('Grey',0.48,0.52,0.57);
#16927=FILL_AREA_STYLE_COLOUR('',#16926);
#16928=FILL_AREA_STYLE('',(#16927));
#16929=SURFACE_STYLE_FILL_AREA(#16928);
#16930=SURFACE_SIDE_STYLE('',(#16929));
#16931=SURFACE_STYLE_USAGE(.BOTH.,#16930);
#16932=PRESENTATION_STYLE_ASSIGNMENT((#16931));
ENDSEC;
END-ISO-10303-21;
